ISO-10303-21;
HEADER;
/* Generated by software containing ST-Developer
 * from STEP Tools, Inc. (www.steptools.com) 
 */

FILE_DESCRIPTION(
/* description */ ('Caster wheel assembly'),
/* implementation_level */ '2;1');

FILE_NAME(
/* name */ 'Wheel bearing retainer (1).step',
/* time_stamp */ '2026-10-28T03:23:56-07:00',
/* author */ (''),
/* organization */ (''),
/* preprocessor_version */ 'ST-DEVELOPER v20.2',
/* originating_system */ 'Autodesk Translation Framework v15.17.0.0',
/* authorisation */ '');

FILE_SCHEMA (('AUTOMOTIVE_DESIGN { 1 0 10303 214 3 1 1 }'));
ENDSEC;

DATA;
#10=MECHANICAL_DESIGN_GEOMETRIC_PRESENTATION_REPRESENTATION('',(#238),#5385);
#194=SHAPE_REPRESENTATION_RELATIONSHIP('SRR','None',#5491,#216);
#216=ADVANCED_BREP_SHAPE_REPRESENTATION('',(#267),#5378);
#238=STYLED_ITEM('',(#5672),#267);
#267=MANIFOLD_SOLID_BREP('Body1',#2666);
#322=FACE_BOUND('',#746,.T.);
#323=FACE_BOUND('',#748,.T.);
#402=PLANE('',#3160);
#403=PLANE('',#3161);
#534=FACE_OUTER_BOUND('',#743,.T.);
#535=FACE_OUTER_BOUND('',#744,.T.);
#536=FACE_OUTER_BOUND('',#745,.T.);
#537=FACE_OUTER_BOUND('',#747,.T.);
#743=EDGE_LOOP('',(#2204,#2205,#2206,#2207));
#744=EDGE_LOOP('',(#2208,#2209,#2210,#2211));
#745=EDGE_LOOP('',(#2212));
#746=EDGE_LOOP('',(#2213));
#747=EDGE_LOOP('',(#2214));
#748=EDGE_LOOP('',(#2215));
#925=LINE('',#4726,#1059);
#926=LINE('',#4732,#1060);
#1059=VECTOR('',#3886,1.1);
#1060=VECTOR('',#3893,1.5);
#1160=CIRCLE('',#3155,1.1);
#1161=CIRCLE('',#3156,1.1);
#1162=CIRCLE('',#3158,1.5);
#1163=CIRCLE('',#3159,1.5);
#1375=VERTEX_POINT('',#4723);
#1376=VERTEX_POINT('',#4725);
#1377=VERTEX_POINT('',#4729);
#1378=VERTEX_POINT('',#4731);
#1670=EDGE_CURVE('',#1375,#1375,#1160,.T.);
#1671=EDGE_CURVE('',#1375,#1376,#925,.T.);
#1672=EDGE_CURVE('',#1376,#1376,#1161,.T.);
#1673=EDGE_CURVE('',#1377,#1377,#1162,.T.);
#1674=EDGE_CURVE('',#1377,#1378,#926,.T.);
#1675=EDGE_CURVE('',#1378,#1378,#1163,.T.);
#2204=ORIENTED_EDGE('',*,*,#1670,.F.);
#2205=ORIENTED_EDGE('',*,*,#1671,.T.);
#2206=ORIENTED_EDGE('',*,*,#1672,.T.);
#2207=ORIENTED_EDGE('',*,*,#1671,.F.);
#2208=ORIENTED_EDGE('',*,*,#1673,.F.);
#2209=ORIENTED_EDGE('',*,*,#1674,.T.);
#2210=ORIENTED_EDGE('',*,*,#1675,.T.);
#2211=ORIENTED_EDGE('',*,*,#1674,.F.);
#2212=ORIENTED_EDGE('',*,*,#1673,.T.);
#2213=ORIENTED_EDGE('',*,*,#1670,.T.);
#2214=ORIENTED_EDGE('',*,*,#1675,.F.);
#2215=ORIENTED_EDGE('',*,*,#1672,.F.);
#2467=CYLINDRICAL_SURFACE('',#3154,1.1);
#2468=CYLINDRICAL_SURFACE('',#3157,1.5);
#2594=ADVANCED_FACE('',(#534),#2467,.F.);
#2595=ADVANCED_FACE('',(#535),#2468,.T.);
#2596=ADVANCED_FACE('',(#536,#322),#402,.T.);
#2597=ADVANCED_FACE('',(#537,#323),#403,.F.);
#2666=CLOSED_SHELL('',(#2594,#2595,#2596,#2597));
#3153=AXIS2_PLACEMENT_3D('',#4721,#3880,#3881);
#3154=AXIS2_PLACEMENT_3D('',#4722,#3882,#3883);
#3155=AXIS2_PLACEMENT_3D('',#4724,#3884,#3885);
#3156=AXIS2_PLACEMENT_3D('',#4727,#3887,#3888);
#3157=AXIS2_PLACEMENT_3D('',#4728,#3889,#3890);
#3158=AXIS2_PLACEMENT_3D('',#4730,#3891,#3892);
#3159=AXIS2_PLACEMENT_3D('',#4733,#3894,#3895);
#3160=AXIS2_PLACEMENT_3D('',#4734,#3896,#3897);
#3161=AXIS2_PLACEMENT_3D('',#4735,#3898,#3899);
#3880=DIRECTION('axis',(0.,0.,1.));
#3881=DIRECTION('refdir',(1.,0.,0.));
#3882=DIRECTION('center_axis',(0.,1.,0.));
#3883=DIRECTION('ref_axis',(1.,0.,0.));
#3884=DIRECTION('center_axis',(0.,-1.,0.));
#3885=DIRECTION('ref_axis',(1.,0.,0.));
#3886=DIRECTION('',(0.,-1.,0.));
#3887=DIRECTION('center_axis',(0.,-1.,0.));
#3888=DIRECTION('ref_axis',(1.,0.,0.));
#3889=DIRECTION('center_axis',(0.,1.,0.));
#3890=DIRECTION('ref_axis',(1.,0.,0.));
#3891=DIRECTION('center_axis',(0.,1.,0.));
#3892=DIRECTION('ref_axis',(1.,0.,0.));
#3893=DIRECTION('',(0.,-1.,0.));
#3894=DIRECTION('center_axis',(0.,1.,0.));
#3895=DIRECTION('ref_axis',(1.,0.,0.));
#3896=DIRECTION('center_axis',(0.,1.,0.));
#3897=DIRECTION('ref_axis',(1.,0.,0.));
#3898=DIRECTION('center_axis',(0.,1.,0.));
#3899=DIRECTION('ref_axis',(1.,0.,0.));
#4721=CARTESIAN_POINT('',(0.,0.,0.));
#4722=CARTESIAN_POINT('Origin',(0.,1.05,4.));
#4723=CARTESIAN_POINT('',(-1.1,1.2,4.));
#4724=CARTESIAN_POINT('Origin',(0.,1.2,4.));
#4725=CARTESIAN_POINT('',(-1.1,1.05,4.));
#4726=CARTESIAN_POINT('',(-1.1,1.05,4.));
#4727=CARTESIAN_POINT('Origin',(0.,1.05,4.));
#4728=CARTESIAN_POINT('Origin',(0.,1.05,4.));
#4729=CARTESIAN_POINT('',(-1.5,1.2,4.));
#4730=CARTESIAN_POINT('Origin',(0.,1.2,4.));
#4731=CARTESIAN_POINT('',(-1.5,1.05,4.));
#4732=CARTESIAN_POINT('',(-1.5,1.05,4.));
#4733=CARTESIAN_POINT('Origin',(0.,1.05,4.));
#4734=CARTESIAN_POINT('Origin',(0.,1.2,4.));
#4735=CARTESIAN_POINT('Origin',(0.,1.05,4.));
#5350=UNCERTAINTY_MEASURE_WITH_UNIT(LENGTH_MEASURE(0.001),#5386,
'DISTANCE_ACCURACY_VALUE',
'Maximum model space distance between geometric entities at asserted c
onnectivities');
#5357=UNCERTAINTY_MEASURE_WITH_UNIT(LENGTH_MEASURE(0.001),#5386,
'DISTANCE_ACCURACY_VALUE',
'Maximum model space distance between geometric entities at asserted c
onnectivities');
#5378=(
GEOMETRIC_REPRESENTATION_CONTEXT(3)
GLOBAL_UNCERTAINTY_ASSIGNED_CONTEXT((#5350))
GLOBAL_UNIT_ASSIGNED_CONTEXT((#5386,#5388,#5389))
REPRESENTATION_CONTEXT('','3D')
);
#5385=(
GEOMETRIC_REPRESENTATION_CONTEXT(3)
GLOBAL_UNCERTAINTY_ASSIGNED_CONTEXT((#5357))
GLOBAL_UNIT_ASSIGNED_CONTEXT((#5386,#5388,#5389))
REPRESENTATION_CONTEXT('','3D')
);
#5386=(
LENGTH_UNIT()
NAMED_UNIT(*)
SI_UNIT(.CENTI.,.METRE.)
);
#5388=(
NAMED_UNIT(*)
PLANE_ANGLE_UNIT()
SI_UNIT($,.RADIAN.)
);
#5389=(
NAMED_UNIT(*)
SI_UNIT($,.STERADIAN.)
SOLID_ANGLE_UNIT()
);
#5410=SHAPE_DEFINITION_REPRESENTATION(#5451,#5491);
#5451=PRODUCT_DEFINITION_SHAPE('',$,#5519);
#5491=SHAPE_REPRESENTATION('',(#3153),#5378);
#5498=PRODUCT_DEFINITION_CONTEXT('part definition',#5581,'design');
#5519=PRODUCT_DEFINITION('Wheel bearing retainer (1)',
'Wheel bearing retainer (1)',#5546,#5498);
#5546=PRODUCT_DEFINITION_FORMATION('',$,#5603);
#5581=APPLICATION_CONTEXT(
'Core Data for Automotive Mechanical Design Process');
#5582=PRODUCT_CONTEXT('part definition',#5581,'mechanical');
#5603=PRODUCT('Wheel bearing retainer (1)','Wheel bearing retainer (1)',
'Wheel bearing retainer (1)',(#5582));
#5666=COLOUR_RGB('Grey',0.48,0.52,0.57);
#5667=FILL_AREA_STYLE_COLOUR('',#5666);
#5668=FILL_AREA_STYLE('',(#5667));
#5669=SURFACE_STYLE_FILL_AREA(#5668);
#5670=SURFACE_SIDE_STYLE('',(#5669));
#5671=SURFACE_STYLE_USAGE(.BOTH.,#5670);
#5672=PRESENTATION_STYLE_ASSIGNMENT((#5671));
ENDSEC;
END-ISO-10303-21;
